ISO-10303-21;
HEADER;
FILE_DESCRIPTION (('STEP AP214'),
    '1' );
FILE_NAME ('Bolt.step',
    '2026-10-24T18:16:00',
    ( '' ),
    ( '' ),
    'SwSTEP 2.0',
    'SolidWorks 2025',
    '' );
FILE_SCHEMA (( 'AUTOMOTIVE_DESIGN' ));
ENDSEC;

DATA;
#113=VERTEX_POINT ( 'NONE', #2354 ) ;
#196=CARTESIAN_POINT ( 'NONE',  ( -1.084824920504545016E-17, 0.000000000000000000, -0.08858267716535432601 ) ) ;
#286=ORIENTED_EDGE ( 'NONE', *, *, #10985, .F. ) ;
#344=VECTOR ( 'NONE', #6500, 39.37007874015748143 ) ;
#361=ORIENTED_EDGE ( 'NONE', *, *, #5853, .T. ) ;
#389=DIRECTION ( 'NONE',  ( 0.000000000000000000, 0.000000000000000000, 1.000000000000000000 ) ) ;
#408=AXIS2_PLACEMENT_3D ( 'NONE', #9723, #13299, #5940 ) ;
#426=VERTEX_POINT ( 'NONE', #5147 ) ;
#429=DIRECTION ( 'NONE',  ( 0.5000000000000001110, 0.000000000000000000, -0.8660254037844385966 ) ) ;
#444=ORIENTED_EDGE ( 'NONE', *, *, #4068, .T. ) ;
#463=MECHANICAL_DESIGN_GEOMETRIC_PRESENTATION_REPRESENTATION('',(#2947),#13453);
#551=ORIENTED_EDGE ( 'NONE', *, *, #10373, .T. ) ;
#565=CARTESIAN_POINT ( 'NONE',  ( -0.05114323250695503725, 0.05905511811023622659, -0.08858267716535432601 ) ) ;
#566=CARTESIAN_POINT ( 'NONE',  ( 0.05114323250695499562, 0.05905511811023622659, -0.08858267716535433989 ) ) ;
#584=AXIS2_PLACEMENT_3D ( 'NONE', #13762, #12668, #13585 ) ;
#601=DIRECTION ( 'NONE',  ( 0.000000000000000000, 0.000000000000000000, 1.000000000000000000 ) ) ;
#617=CARTESIAN_POINT ( 'NONE',  ( 0.000000000000000000, 0.05905511811023623353, 0.04527559055118110520 ) ) ;
#646=VERTEX_POINT ( 'NONE', #6349 ) ;
#653=AXIS2_PLACEMENT_3D ( 'NONE', #565, #6348, #429 ) ;
#657=ORIENTED_EDGE ( 'NONE', *, *, #8641, .T. ) ;
#672=DIRECTION ( 'NONE',  ( -0.000000000000000000, -1.000000000000000000, -0.000000000000000000 ) ) ;
#684=AXIS2_PLACEMENT_3D ( 'NONE', #10604, #15073, #15394 ) ;
#694=ORIENTED_EDGE ( 'NONE', *, *, #10855, .T. ) ;
#719=AXIS2_PLACEMENT_3D ( 'NONE', #11281, #5307, #9175 ) ;
#742=DIRECTION ( 'NONE',  ( -0.8660254037844385966, 0.000000000000000000, -0.5000000000000001110 ) ) ;
#748=VERTEX_POINT ( 'NONE', #14368 ) ;
#775=PRODUCT_DEFINITION_SHAPE ( 'NONE', 'NONE',  #3339 ) ;
#795=EDGE_CURVE ( 'NONE', #13551, #646, #5417, .T. ) ;
#813=DIRECTION ( 'NONE',  ( -0.8660254037844385966, 0.000000000000000000, 0.5000000000000002220 ) ) ;
#814=ORIENTED_EDGE ( 'NONE', *, *, #8460, .F. ) ;
#821=CARTESIAN_POINT ( 'NONE',  ( 0.1022864650139100745, 0.05905511811023622659, 1.563012696487738457E-17 ) ) ;
#822=ADVANCED_FACE ( 'NONE', ( #9035 ), #7844, .F. ) ;
#823=CARTESIAN_POINT ( 'NONE',  ( 0.000000000000000000, 0.4133858267716535306, -0.03937007874015747977 ) ) ;
#891=PLANE ( 'NONE',  #2622 ) ;
#892=AXIS2_PLACEMENT_3D ( 'NONE', #1259, #7211, #9414 ) ;
#932=( GEOMETRIC_REPRESENTATION_CONTEXT ( 3 ) GLOBAL_UNCERTAINTY_ASSIGNED_CONTEXT ( ( #2508 ) ) GLOBAL_UNIT_ASSIGNED_CONTEXT ( ( #2686, #3784, #14587 ) ) REPRESENTATION_CONTEXT ( 'NONE', 'WORKASPACE' ) );
#1001=CARTESIAN_POINT ( 'NONE',  ( 0.000000000000000000, 0.4133858267716535306, 0.000000000000000000 ) ) ;
#1045=CARTESIAN_POINT ( 'NONE',  ( -0.07874015748031494566, 0.1685051786281938357, 0.03937007874015747977 ) ) ;
#1055=FACE_OUTER_BOUND ( 'NONE', #5530, .T. ) ;
#1067=FACE_OUTER_BOUND ( 'NONE', #9501, .T. ) ;
#1077=( BOUNDED_CURVE ( )  B_SPLINE_CURVE ( 3, ( #8250, #15379, #1045, #14277 ),
 .UNSPECIFIED., .F., .T. ) 
 B_SPLINE_CURVE_WITH_KNOTS ( ( 4, 4 ),
 ( 4.712388980384689674, 7.853981633974482790 ),
 .UNSPECIFIED. ) 
 CURVE ( )  GEOMETRIC_REPRESENTATION_ITEM ( )  RATIONAL_B_SPLINE_CURVE ( ( 1.000000000000000000, 0.3333333333333333703, 0.3333333333333333703, 1.000000000000000000 ) ) 
 REPRESENTATION_ITEM ( '' )  );
#1087=EDGE_CURVE ( 'NONE', #1730, #1174, #1165, .T. ) ;
#1165=CIRCLE ( 'NONE', #408, 0.04527559055118110520 ) ;
#1170=DIRECTION ( 'NONE',  ( -1.000000000000000000, 0.000000000000000000, 0.000000000000000000 ) ) ;
#1174=VERTEX_POINT ( 'NONE', #617 ) ;
#1207=ADVANCED_FACE ( 'NONE', ( #8928 ), #5376, .T. ) ;
#1214=EDGE_CURVE ( 'NONE', #11540, #7421, #7608, .T. ) ;
#1215=LINE ( 'NONE', #4873, #10383 ) ;
#1230=CARTESIAN_POINT ( 'NONE',  ( 4.821444091131311524E-18, 0.4133858267716535306, 0.03937007874015747977 ) ) ;
#1234=CARTESIAN_POINT ( 'NONE',  ( 0.1022864650139100745, 0.05905511811023622659, 1.563012696487738457E-17 ) ) ;
#1247=DIRECTION ( 'NONE',  ( 0.000000000000000000, 1.000000000000000000, 0.000000000000000000 ) ) ;
#1259=CARTESIAN_POINT ( 'NONE',  ( 5.544660704801008561E-18, 0.06496062992125986590, -0.04527559055118110520 ) ) ;
#1273=CARTESIAN_POINT ( 'NONE',  ( -0.05114323250695503725, 0.000000000000000000, -0.08858267716535432601 ) ) ;
#1400=VECTOR ( 'NONE', #8450, 39.37007874015748143 ) ;
#1480=EDGE_LOOP ( 'NONE', ( #4243, #361, #13753, #4015 ) ) ;
#1529=EDGE_LOOP ( 'NONE', ( #10287, #657, #4566, #2023 ) ) ;
#1562=ADVANCED_FACE ( 'NONE', ( #2231 ), #10531, .F. ) ;
#1578=ADVANCED_FACE ( 'NONE', ( #1055 ), #4420, .F. ) ;
#1643=LINE ( 'NONE', #2798, #11183 ) ;
#1730=VERTEX_POINT ( 'NONE', #4409 ) ;
#1731=VERTEX_POINT ( 'NONE', #11473 ) ;
#1751=CARTESIAN_POINT ( 'NONE',  ( -0.05114323250695503725, 0.000000000000000000, -0.08858267716535432601 ) ) ;
#1788=LINE ( 'NONE', #5525, #4435 ) ;
#1830=EDGE_LOOP ( 'NONE', ( #3385, #4258 ) ) ;
#1834=ORIENTED_EDGE ( 'NONE', *, *, #6073, .F. ) ;
#1944=VECTOR ( 'NONE', #10157, 39.37007874015748143 ) ;
#1981=EDGE_CURVE ( 'NONE', #10078, #1174, #7695, .T. ) ;
#1998=ORIENTED_EDGE ( 'NONE', *, *, #7410, .F. ) ;
#2000=CARTESIAN_POINT ( 'NONE',  ( 0.000000000000000000, 0.4133858267716535306, 0.000000000000000000 ) ) ;
#2004=LINE ( 'NONE', #823, #344 ) ;
#2014=CARTESIAN_POINT ( 'NONE',  ( 0.000000000000000000, 0.06496062992125986590, 0.000000000000000000 ) ) ;
#2018=ORIENTED_EDGE ( 'NONE', *, *, #5129, .F. ) ;
#2023=ORIENTED_EDGE ( 'NONE', *, *, #13199, .F. ) ;
#2045=DIRECTION ( 'NONE',  ( 0.000000000000000000, 0.000000000000000000, -1.000000000000000000 ) ) ;
#2069=( NAMED_UNIT ( * ) PLANE_ANGLE_UNIT ( ) SI_UNIT ( $, .RADIAN. ) );
#2129=ORIENTED_EDGE ( 'NONE', *, *, #12254, .F. ) ;
#2141=LINE ( 'NONE', #11539, #14134 ) ;
#2162=AXIS2_PLACEMENT_3D ( 'NONE', #2880, #5148, #389 ) ;
#2192=ORIENTED_EDGE ( 'NONE', *, *, #795, .T. ) ;
#2231=FACE_OUTER_BOUND ( 'NONE', #10129, .T. ) ;
#2352=ORIENTED_EDGE ( 'NONE', *, *, #10559, .F. ) ;
#2354=CARTESIAN_POINT ( 'NONE',  ( 0.1022864650139100745, 0.000000000000000000, 1.563012696487738457E-17 ) ) ;
#2446=CARTESIAN_POINT ( 'NONE',  ( -0.05114323250695500950, 0.05905511811023622659, 0.08858267716535433989 ) ) ;
#2508=UNCERTAINTY_MEASURE_WITH_UNIT (LENGTH_MEASURE( 1.000000000000000082E-05 ), #2686, 'distance_accuracy_value', 'NONE');
#2522=CARTESIAN_POINT ( 'NONE',  ( 0.000000000000000000, 0.4133858267716535306, 0.03543307086614173179 ) ) ;
#2550=CARTESIAN_POINT ( 'NONE',  ( 4.821444091131311524E-18, 0.1692468441617604180, 0.03937007874015747977 ) ) ;
#2559=VERTEX_POINT ( 'NONE', #13749 ) ;
#2622=AXIS2_PLACEMENT_3D ( 'NONE', #3403, #10689, #15386 ) ;
#2630=ORIENTED_EDGE ( 'NONE', *, *, #5413, .F. ) ;
#2631=VERTEX_POINT ( 'NONE', #196 ) ;
#2686=( CONVERSION_BASED_UNIT ( 'INCH', #2757 ) LENGTH_UNIT ( ) NAMED_UNIT ( #10348 ) );
#2689=VERTEX_POINT ( 'NONE', #9895 ) ;
#2722=CARTESIAN_POINT ( 'NONE',  ( 0.000000000000000000, 0.1692468441617604180, -0.03937007874015747977 ) ) ;
#2741=DIRECTION ( 'NONE',  ( 0.5000000000000001110, 0.000000000000000000, -0.8660254037844385966 ) ) ;
#2757=LENGTH_MEASURE_WITH_UNIT ( LENGTH_MEASURE( 0.02539999999999999897 ), #7375 );
#2758=ADVANCED_BREP_SHAPE_REPRESENTATION ( '', ( #9613, #14728, #11481 ), #14478 ) ;
#2798=CARTESIAN_POINT ( 'NONE',  ( 0.000000000000000000, 0.4133858267716535306, -0.03937007874015747977 ) ) ;
#2819=AXIS2_PLACEMENT_3D ( 'NONE', #12725, #12788, #2045 ) ;
#2834=VECTOR ( 'NONE', #5316, 39.37007874015748854 ) ;
#2858=AXIS2_PLACEMENT_3D ( 'NONE', #7016, #9290, #14066 ) ;
#2859=CLOSED_SHELL ( 'NONE', ( #5798, #3468, #6553, #7889, #1207, #4927, #5474, #1562, #822, #6358, #1578, #8350, #10726, #7898, #7963, #11257, #15332 ) ) ;
#2880=CARTESIAN_POINT ( 'NONE',  ( 0.000000000000000000, 0.4094488188976377896, 0.000000000000000000 ) ) ;
#2909=DIRECTION ( 'NONE',  ( 0.000000000000000000, 0.000000000000000000, 1.000000000000000000 ) ) ;
#2947=STYLED_ITEM('',(#15533),#14728);
#3108=AXIS2_PLACEMENT_3D ( 'NONE', #11941, #12791, #9339 ) ;
#3113=AXIS2_PLACEMENT_3D ( 'NONE', #2014, #11334, #6542 ) ;
#3124=EDGE_LOOP ( 'NONE', ( #551, #8769, #10127, #3337 ) ) ;
#3132=PRODUCT_DEFINITION_CONTEXT ( 'detailed design', #14004, 'design' ) ;
#3158=CYLINDRICAL_SURFACE ( 'NONE', #2819, 0.03937007874015747977 ) ;
#3182=AXIS2_PLACEMENT_3D ( 'NONE', #10293, #813, #7003 ) ;
#3270=PLANE ( 'NONE',  #4356 ) ;
#3271=CARTESIAN_POINT ( 'NONE',  ( 0.000000000000000000, 0.4133858267716535306, 0.000000000000000000 ) ) ;
#3292=APPLICATION_CONTEXT ( 'automotive_design' ) ;
#3315=EDGE_LOOP ( 'NONE', ( #6806, #8194, #8052, #694, #6743, #3591 ) ) ;
#3337=ORIENTED_EDGE ( 'NONE', *, *, #5954, .T. ) ;
#3339=PRODUCT_DEFINITION ( 'UNKNOWN', '', #5596, #3132 ) ;
#3345=VECTOR ( 'NONE', #5304, 39.37007874015748854 ) ;
#3371=DIRECTION ( 'NONE',  ( -1.000000000000000000, 0.000000000000000000, 1.669238443041289401E-16 ) ) ;
#3385=ORIENTED_EDGE ( 'NONE', *, *, #6002, .F. ) ;
#3403=CARTESIAN_POINT ( 'NONE',  ( 0.000000000000000000, 0.05905511811023622659, 0.000000000000000000 ) ) ;
#3442=DIRECTION ( 'NONE',  ( 0.000000000000000000, 0.000000000000000000, 1.000000000000000000 ) ) ;
#3468=ADVANCED_FACE ( 'NONE', ( #10946 ), #7822, .T. ) ;
#3513=DIRECTION ( 'NONE',  ( 0.000000000000000000, 0.000000000000000000, 1.000000000000000000 ) ) ;
#3515=DIRECTION ( 'NONE',  ( -0.000000000000000000, -1.000000000000000000, -0.000000000000000000 ) ) ;
#3591=ORIENTED_EDGE ( 'NONE', *, *, #5413, .T. ) ;
#3696=ORIENTED_EDGE ( 'NONE', *, *, #12090, .T. ) ;
#3699=AXIS2_PLACEMENT_3D ( 'NONE', #10195, #10034, #2909 ) ;
#3703=EDGE_CURVE ( 'NONE', #7421, #4739, #2004, .T. ) ;
#3761=ORIENTED_EDGE ( 'NONE', *, *, #6814, .F. ) ;
#3770=CARTESIAN_POINT ( 'NONE',  ( -0.05114323250695503725, 0.05905511811023622659, -0.08858267716535432601 ) ) ;
#3784=( NAMED_UNIT ( * ) PLANE_ANGLE_UNIT ( ) SI_UNIT ( $, .RADIAN. ) );
#3796=EDGE_CURVE ( 'NONE', #2559, #2631, #5244, .T. ) ;
#3814=VERTEX_POINT ( 'NONE', #1234 ) ;
#3843=LINE ( 'NONE', #8713, #13967 ) ;
#3863=LINE ( 'NONE', #8793, #6384 ) ;
#3959=VECTOR ( 'NONE', #3371, 39.37007874015748143 ) ;
#4015=ORIENTED_EDGE ( 'NONE', *, *, #1981, .F. ) ;
#4066=TOROIDAL_SURFACE ( 'NONE', #12585, 0.03543307086614173179, 0.003937007874015747977 ) ;
#4068=EDGE_CURVE ( 'NONE', #646, #1731, #4518, .T. ) ;
#4100=DIRECTION ( 'NONE',  ( 0.000000000000000000, 0.000000000000000000, 1.000000000000000000 ) ) ;
#4104=ORIENTED_EDGE ( 'NONE', *, *, #3703, .T. ) ;
#4119=AXIS2_PLACEMENT_3D ( 'NONE', #12308, #6252, #11125 ) ;
#4135=DIRECTION ( 'NONE',  ( -0.000000000000000000, -1.000000000000000000, -0.000000000000000000 ) ) ;
#4216=DIRECTION ( 'NONE',  ( -1.000000000000000000, 0.000000000000000000, -0.000000000000000000 ) ) ;
#4243=ORIENTED_EDGE ( 'NONE', *, *, #4928, .F. ) ;
#4254=DIRECTION ( 'NONE',  ( -0.000000000000000000, -1.000000000000000000, -0.000000000000000000 ) ) ;
#4258=ORIENTED_EDGE ( 'NONE', *, *, #12409, .F. ) ;
#4264=DIRECTION ( 'NONE',  ( 0.000000000000000000, 0.000000000000000000, 1.000000000000000000 ) ) ;
#4286=VERTEX_POINT ( 'NONE', #5030 ) ;
#4356=AXIS2_PLACEMENT_3D ( 'NONE', #9070, #6628, #4216 ) ;
#4359=EDGE_CURVE ( 'NONE', #113, #7319, #14901, .T. ) ;
#4409=CARTESIAN_POINT ( 'NONE',  ( 5.544660704801008561E-18, 0.05905511811023623353, -0.04527559055118110520 ) ) ;
#4414=FACE_OUTER_BOUND ( 'NONE', #3315, .T. ) ;
#4420=PLANE ( 'NONE',  #684 ) ;
#4435=VECTOR ( 'NONE', #4135, 39.37007874015748143 ) ;
#4439=ORIENTED_EDGE ( 'NONE', *, *, #8460, .T. ) ;
#4470=DIRECTION ( 'NONE',  ( 0.000000000000000000, 0.000000000000000000, 1.000000000000000000 ) ) ;
#4493=( NAMED_UNIT ( * ) SI_UNIT ( $, .STERADIAN. ) SOLID_ANGLE_UNIT ( ) );
#4506=CYLINDRICAL_SURFACE ( 'NONE', #14381, 0.03937007874015747977 ) ;
#4518=LINE ( 'NONE', #9299, #9862 ) ;
#4566=ORIENTED_EDGE ( 'NONE', *, *, #12977, .F. ) ;
#4598=CARTESIAN_POINT ( 'NONE',  ( 0.000000000000000000, 0.000000000000000000, 0.000000000000000000 ) ) ;
#4642=EDGE_CURVE ( 'NONE', #4286, #10078, #14259, .T. ) ;
#4652=VECTOR ( 'NONE', #13763, 39.37007874015748854 ) ;
#4666=DIRECTION ( 'NONE',  ( 0.000000000000000000, 1.000000000000000000, 0.000000000000000000 ) ) ;
#4706=CARTESIAN_POINT ( 'NONE',  ( 0.05114323250695499562, 0.05905511811023622659, -0.08858267716535433989 ) ) ;
#4739=VERTEX_POINT ( 'NONE', #11266 ) ;
#4747=CYLINDRICAL_SURFACE ( 'NONE', #9125, 0.03937007874015747977 ) ;
#4761=CARTESIAN_POINT ( 'NONE',  ( -0.05114323250695500950, 0.05905511811023622659, 0.08858267716535433989 ) ) ;
#4774=CARTESIAN_POINT ( 'NONE',  ( 0.000000000000000000, 0.06496062992125986590, -0.03937007874015747977 ) ) ;
#4796=ORIENTED_EDGE ( 'NONE', *, *, #3703, .F. ) ;
#4805=DIRECTION ( 'NONE',  ( -0.000000000000000000, -1.000000000000000000, -0.000000000000000000 ) ) ;
#4873=CARTESIAN_POINT ( 'NONE',  ( 0.05114323250695503031, 0.000000000000000000, 0.08858267716535433989 ) ) ;
#4882=CIRCLE ( 'NONE', #9653, 0.03543307086614173179 ) ;
#4927=ADVANCED_FACE ( 'NONE', ( #15098 ), #3270, .F. ) ;
#4928=EDGE_CURVE ( 'NONE', #12623, #10078, #15117, .T. ) ;
#4972=ORIENTED_EDGE ( 'NONE', *, *, #13510, .F. ) ;
#5030=CARTESIAN_POINT ( 'NONE',  ( 4.821444091131311524E-18, 0.1692468441617604180, 0.03937007874015747977 ) ) ;
#5129=EDGE_CURVE ( 'NONE', #11540, #4286, #9827, .T. ) ;
#5139=PLANE ( 'NONE',  #10910 ) ;
#5147=CARTESIAN_POINT ( 'NONE',  ( 0.05114323250695499562, 0.05905511811023622659, -0.08858267716535433989 ) ) ;
#5148=DIRECTION ( 'NONE',  ( -0.000000000000000000, -1.000000000000000000, -0.000000000000000000 ) ) ;
#5151=ORIENTED_EDGE ( 'NONE', *, *, #795, .F. ) ;
#5217=ORIENTED_EDGE ( 'NONE', *, *, #12254, .T. ) ;
#5232=ORIENTED_EDGE ( 'NONE', *, *, #4068, .F. ) ;
#5244=LINE ( 'NONE', #11973, #2834 ) ;
#5274=FACE_OUTER_BOUND ( 'NONE', #9737, .T. ) ;
#5304=DIRECTION ( 'NONE',  ( -0.5000000000000001110, 0.000000000000000000, -0.8660254037844384856 ) ) ;
#5307=DIRECTION ( 'NONE',  ( -0.000000000000000000, 1.000000000000000000, 0.000000000000000000 ) ) ;
#5316=DIRECTION ( 'NONE',  ( -1.060575238724908024E-16, -0.4999999999999979461, -0.8660254037844397068 ) ) ;
#5330=DIRECTION ( 'NONE',  ( 0.000000000000000000, -1.000000000000000000, -0.000000000000000000 ) ) ;
#5376=CYLINDRICAL_SURFACE ( 'NONE', #15391, 0.03937007874015747977 ) ;
#5413=EDGE_CURVE ( 'NONE', #13551, #6722, #2141, .T. ) ;
#5417=LINE ( 'NONE', #6667, #7156 ) ;
#5435=ORIENTED_EDGE ( 'NONE', *, *, #4359, .F. ) ;
#5441=DIRECTION ( 'NONE',  ( 1.000000000000000000, 0.000000000000000000, 0.000000000000000000 ) ) ;
#5474=ADVANCED_FACE ( 'NONE', ( #5724 ), #6674, .F. ) ;
#5491=LINE ( 'NONE', #12861, #12173 ) ;
#5525=CARTESIAN_POINT ( 'NONE',  ( 0.05114323250695503031, 0.05905511811023622659, 0.08858267716535433989 ) ) ;
#5530=EDGE_LOOP ( 'NONE', ( #444, #14446, #2630, #2192 ) ) ;
#5584=SHAPE_REPRESENTATION_RELATIONSHIP ( 'NONE' , 'NONE' ,  #7785, #2758 ) ;
#5596=PRODUCT_DEFINITION_FORMATION_WITH_SPECIFIED_SOURCE ( 'ANY', '', #8693, .NOT_KNOWN. ) ;
#5607=DIRECTION ( 'NONE',  ( 0.5000000000000002220, 0.000000000000000000, 0.8660254037844384856 ) ) ;
#5608=CIRCLE ( 'NONE', #4119, 0.08858267716535432601 ) ;
#5660=EDGE_LOOP ( 'NONE', ( #4439, #4972, #7779, #6215 ) ) ;
#5687=AXIS2_PLACEMENT_3D ( 'NONE', #14398, #8439, #13449 ) ;
#5724=FACE_OUTER_BOUND ( 'NONE', #5660, .T. ) ;
#5747=DIRECTION ( 'NONE',  ( -0.000000000000000000, -1.000000000000000000, -0.000000000000000000 ) ) ;
#5798=ADVANCED_FACE ( 'NONE', ( #12844 ), #7376, .F. ) ;
#5817=FACE_OUTER_BOUND ( 'NONE', #13946, .T. ) ;
#5853=EDGE_CURVE ( 'NONE', #12623, #1730, #7885, .T. ) ;
#5906=LENGTH_MEASURE_WITH_UNIT ( LENGTH_MEASURE( 0.02539999999999999897 ), #14147 );
#5923=DIRECTION ( 'NONE',  ( 0.000000000000000000, 0.000000000000000000, 1.000000000000000000 ) ) ;
#5924=CARTESIAN_POINT ( 'NONE',  ( 0.05114323250695503031, 0.000000000000000000, 0.08858267716535433989 ) ) ;
#5940=DIRECTION ( 'NONE',  ( 0.000000000000000000, 0.000000000000000000, 1.000000000000000000 ) ) ;
#5954=EDGE_CURVE ( 'NONE', #6722, #1731, #12533, .T. ) ;
#6002=EDGE_CURVE ( 'NONE', #11019, #2631, #6617, .T. ) ;
#6023=DIRECTION ( 'NONE',  ( -0.5000000000000001110, 0.000000000000000000, 0.8660254037844385966 ) ) ;
#6073=EDGE_CURVE ( 'NONE', #4286, #4739, #13284, .T. ) ;
#6215=ORIENTED_EDGE ( 'NONE', *, *, #9977, .T. ) ;
#6235=ORIENTED_EDGE ( 'NONE', *, *, #10373, .F. ) ;
#6248=ORIENTED_EDGE ( 'NONE', *, *, #12230, .T. ) ;
#6252=DIRECTION ( 'NONE',  ( 0.000000000000000000, 1.000000000000000000, 0.000000000000000000 ) ) ;
#6268=EDGE_CURVE ( 'NONE', #3814, #426, #11491, .T. ) ;
#6291=DIRECTION ( 'NONE',  ( 0.000000000000000000, -0.000000000000000000, 1.000000000000000000 ) ) ;
#6302=AXIS2_PLACEMENT_3D ( 'NONE', #11317, #11253, #601 ) ;
#6348=DIRECTION ( 'NONE',  ( 0.8660254037844385966, -0.000000000000000000, 0.5000000000000001110 ) ) ;
#6349=CARTESIAN_POINT ( 'NONE',  ( -0.1022864650139100884, 0.000000000000000000, -1.048351444896847144E-20 ) ) ;
#6358=ADVANCED_FACE ( 'NONE', ( #12183 ), #11142, .F. ) ;
#6377=AXIS2_PLACEMENT_3D ( 'NONE', #11012, #1170, #5923 ) ;
#6381=CARTESIAN_POINT ( 'NONE',  ( 0.07874015748031494566, 0.1699885096953269725, -0.03937007874015747283 ) ) ;
#6384=VECTOR ( 'NONE', #13425, 39.37007874015748143 ) ;
#6432=EDGE_CURVE ( 'NONE', #6722, #8823, #3863, .T. ) ;
#6433=ORIENTED_EDGE ( 'NONE', *, *, #1087, .T. ) ;
#6470=EDGE_LOOP ( 'NONE', ( #3696, #6433 ) ) ;
#6500=DIRECTION ( 'NONE',  ( -0.000000000000000000, -1.000000000000000000, -0.000000000000000000 ) ) ;
#6530=EDGE_CURVE ( 'NONE', #2559, #11019, #5491, .T. ) ;
#6542=DIRECTION ( 'NONE',  ( 0.000000000000000000, 0.000000000000000000, 1.000000000000000000 ) ) ;
#6553=ADVANCED_FACE ( 'NONE', ( #8006 ), #3158, .T. ) ;
#6607=CLOSED_SHELL ( 'NONE', ( #9187, #11543, #8946 ) ) ;
#6614=ORIENTED_EDGE ( 'NONE', *, *, #13199, .T. ) ;
#6617=CIRCLE ( 'NONE', #10396, 0.08858267716535432601 ) ;
#6628=DIRECTION ( 'NONE',  ( 0.000000000000000000, 0.000000000000000000, -1.000000000000000000 ) ) ;
#6651=FACE_OUTER_BOUND ( 'NONE', #12926, .T. ) ;
#6667=CARTESIAN_POINT ( 'NONE',  ( -0.1022864650139100884, 0.05905511811023622659, -1.048351444896847144E-20 ) ) ;
#6670=CARTESIAN_POINT ( 'NONE',  ( 0.000000000000000000, 0.05905511811023622659, 0.000000000000000000 ) ) ;
#6674=PLANE ( 'NONE',  #7606 ) ;
#6722=VERTEX_POINT ( 'NONE', #2446 ) ;
#6726=EDGE_CURVE ( 'NONE', #12058, #646, #12013, .T. ) ;
#6743=ORIENTED_EDGE ( 'NONE', *, *, #6814, .T. ) ;
#6781=CARTESIAN_POINT ( 'NONE',  ( 4.821444091131311524E-18, 0.06496062992125986590, 0.03937007874015747977 ) ) ;
#6806=ORIENTED_EDGE ( 'NONE', *, *, #6432, .T. ) ;
#6814=EDGE_CURVE ( 'NONE', #2689, #13551, #8828, .T. ) ;
#6846=FACE_OUTER_BOUND ( 'NONE', #7605, .T. ) ;
#6877=VECTOR ( 'NONE', #3515, 39.37007874015748143 ) ;
#6883=ORIENTED_EDGE ( 'NONE', *, *, #6073, .T. ) ;
#6932=CARTESIAN_POINT ( 'NONE',  ( 0.05114323250695499562, 0.000000000000000000, -0.08858267716535433989 ) ) ;
#6940=DIRECTION ( 'NONE',  ( -0.000000000000000000, -1.000000000000000000, -0.000000000000000000 ) ) ;
#7003=DIRECTION ( 'NONE',  ( 0.5000000000000001110, 0.000000000000000000, 0.8660254037844384856 ) ) ;
#7016=CARTESIAN_POINT ( 'NONE',  ( 0.000000000000000000, 0.4133858267716535306, 0.000000000000000000 ) ) ;
#7101=DIRECTION ( 'NONE',  ( 0.000000000000000000, 1.000000000000000000, 0.000000000000000000 ) ) ;
#7109=ORIENTED_EDGE ( 'NONE', *, *, #12230, .F. ) ;
#7156=VECTOR ( 'NONE', #11380, 39.37007874015748143 ) ;
#7176=DIRECTION ( 'NONE',  ( -0.000000000000000000, -1.000000000000000000, -0.000000000000000000 ) ) ;
#7198=ORIENTED_EDGE ( 'NONE', *, *, #3796, .F. ) ;
#7211=DIRECTION ( 'NONE',  ( 1.000000000000000000, 0.000000000000000000, 1.224646799147353207E-16 ) ) ;
#7319=VERTEX_POINT ( 'NONE', #6932 ) ;
#7369=EDGE_LOOP ( 'NONE', ( #11485, #10745, #6883, #4796 ) ) ;
#7375=( LENGTH_UNIT ( ) NAMED_UNIT ( * ) SI_UNIT ( $, .METRE. ) );
#7376=TOROIDAL_SURFACE ( 'NONE', #13635, 0.04527559055118110520, 0.005905511811023621965 ) ;
#7410=EDGE_CURVE ( 'NONE', #748, #14826, #13858, .T. ) ;
#7421=VERTEX_POINT ( 'NONE', #12808 ) ;
#7480=ORIENTED_EDGE ( 'NONE', *, *, #7410, .T. ) ;
#7499=ORIENTED_EDGE ( 'NONE', *, *, #6726, .T. ) ;
#7559=ORIENTED_EDGE ( 'NONE', *, *, #8727, .F. ) ;
#7563=DIRECTION ( 'NONE',  ( -0.000000000000000000, -1.000000000000000000, -0.000000000000000000 ) ) ;
#7598=DIRECTION ( 'NONE',  ( 1.224646799147353207E-16, 0.000000000000000000, -1.000000000000000000 ) ) ;
#7605=EDGE_LOOP ( 'NONE', ( #2018, #13523, #4104, #6248 ) ) ;
#7606=AXIS2_PLACEMENT_3D ( 'NONE', #11474, #742, #8544 ) ;
#7608=CIRCLE ( 'NONE', #2162, 0.03937007874015747977 ) ;
#7615=DIRECTION ( 'NONE',  ( 1.000000000000000000, 0.000000000000000000, -1.669238443041289155E-16 ) ) ;
#7695=CIRCLE ( 'NONE', #3699, 0.005905511811023620231 ) ;
#7715=ORIENTED_EDGE ( 'NONE', *, *, #6726, .F. ) ;
#7779=ORIENTED_EDGE ( 'NONE', *, *, #14246, .F. ) ;
#7785=SHAPE_REPRESENTATION ( 'Bolt', ( #11481 ), #14478 ) ;
#7822=TOROIDAL_SURFACE ( 'NONE', #6302, 0.03543307086614173179, 0.003937007874015747977 ) ;
#7832=VECTOR ( 'NONE', #10084, 39.37007874015748143 ) ;
#7844=PLANE ( 'NONE',  #10399 ) ;
#7862=VECTOR ( 'NONE', #10567, 39.37007874015748143 ) ;
#7885=CIRCLE ( 'NONE', #892, 0.005905511811023620231 ) ;
#7889=ADVANCED_FACE ( 'NONE', ( #1067 ), #4747, .T. ) ;
#7898=ADVANCED_FACE ( 'NONE', ( #6846 ), #4506, .T. ) ;
#7903=EDGE_LOOP ( 'NONE', ( #7499, #5151, #3761, #11138 ) ) ;
#7917=DIRECTION ( 'NONE',  ( -0.000000000000000000, 1.000000000000000000, 0.000000000000000000 ) ) ;
#7963=ADVANCED_FACE ( 'NONE', ( #5817 ), #12980, .T. ) ;
#7981=CARTESIAN_POINT ( 'NONE',  ( 4.339299682018179909E-18, 0.4094488188976377896, -0.03543307086614173179 ) ) ;
#8006=FACE_OUTER_BOUND ( 'NONE', #7369, .T. ) ;
#8052=ORIENTED_EDGE ( 'NONE', *, *, #6268, .T. ) ;
#8077=EDGE_CURVE ( 'NONE', #7421, #11540, #8126, .T. ) ;
#8100=AXIS2_PLACEMENT_3D ( 'NONE', #2000, #4666, #11552 ) ;
#8126=CIRCLE ( 'NONE', #14869, 0.03937007874015747977 ) ;
#8135=DIRECTION ( 'NONE',  ( 0.000000000000000000, 0.000000000000000000, 1.000000000000000000 ) ) ;
#8194=ORIENTED_EDGE ( 'NONE', *, *, #14246, .T. ) ;
#8224=DIRECTION ( 'NONE',  ( -0.000000000000000000, -1.000000000000000000, -0.000000000000000000 ) ) ;
#8250=CARTESIAN_POINT ( 'NONE',  ( 0.000000000000000000, 0.1692468441617604180, -0.03937007874015747977 ) ) ;
#8274=DIRECTION ( 'NONE',  ( 0.000000000000000000, 0.000000000000000000, 1.000000000000000000 ) ) ;
#8317=ORIENTED_EDGE ( 'NONE', *, *, #3796, .T. ) ;
#8350=ADVANCED_FACE ( 'NONE', ( #14130, #4414 ), #891, .T. ) ;
#8357=FACE_OUTER_BOUND ( 'NONE', #15090, .T. ) ;
#8431=STYLED_ITEM('',(#15533),#9613);
#8439=DIRECTION ( 'NONE',  ( -0.000000000000000000, 1.000000000000000000, 0.000000000000000000 ) ) ;
#8450=DIRECTION ( 'NONE',  ( -1.000000000000000000, 0.000000000000000000, 1.669238443041289401E-16 ) ) ;
#8460=EDGE_CURVE ( 'NONE', #11277, #113, #1215, .T. ) ;
#8544=DIRECTION ( 'NONE',  ( -0.5000000000000001110, 0.000000000000000000, 0.8660254037844385966 ) ) ;
#8578=FACE_OUTER_BOUND ( 'NONE', #11842, .T. ) ;
#8618=AXIS2_PLACEMENT_3D ( 'NONE', #6670, #5330, #10284 ) ;
#8641=EDGE_CURVE ( 'NONE', #7421, #748, #10897, .T. ) ;
#8693=PRODUCT ( 'Bolt', 'Bolt', '', ( #12493 ) ) ;
#8713=CARTESIAN_POINT ( 'NONE',  ( -0.05114323250695503725, 0.05905511811023622659, -0.08858267716535432601 ) ) ;
#8727=EDGE_CURVE ( 'NONE', #7319, #12058, #11671, .T. ) ;
#8746=LINE ( 'NONE', #11489, #1944 ) ;
#8769=ORIENTED_EDGE ( 'NONE', *, *, #9977, .F. ) ;
#8793=CARTESIAN_POINT ( 'NONE',  ( -0.05114323250695500950, 0.05905511811023622659, 0.08858267716535433989 ) ) ;
#8814=CARTESIAN_POINT ( 'NONE',  ( 0.07874015748031494566, 0.1699885096953269725, 0.03937007874015747977 ) ) ;
#8823=VERTEX_POINT ( 'NONE', #10643 ) ;
#8828=LINE ( 'NONE', #3770, #7832 ) ;
#8928=FACE_OUTER_BOUND ( 'NONE', #9331, .T. ) ;
#8946=ADVANCED_FACE ( 'NONE', ( #11018 ), #5139, .F. ) ;
#8952=PLANE ( 'NONE',  #719 ) ;
#8975=CARTESIAN_POINT ( 'NONE',  ( -0.1022864650139100884, 0.05905511811023622659, -1.048351444896847144E-20 ) ) ;
#9002=DIRECTION ( 'NONE',  ( 0.000000000000000000, 0.000000000000000000, -1.000000000000000000 ) ) ;
#9015=ORIENTED_EDGE ( 'NONE', *, *, #6530, .F. ) ;
#9035=FACE_OUTER_BOUND ( 'NONE', #10562, .T. ) ;
#9070=CARTESIAN_POINT ( 'NONE',  ( -0.05114323250695500950, 0.05905511811023622659, 0.08858267716535433989 ) ) ;
#9125=AXIS2_PLACEMENT_3D ( 'NONE', #11558, #6940, #12812 ) ;
#9175=DIRECTION ( 'NONE',  ( 0.000000000000000000, -0.000000000000000000, 1.000000000000000000 ) ) ;
#9180=MECHANICAL_DESIGN_GEOMETRIC_PRESENTATION_REPRESENTATION('',(#8431),#932);
#9187=ADVANCED_FACE ( 'NONE', ( #10774 ), #14927, .T. ) ;
#9251=CARTESIAN_POINT ( 'NONE',  ( 0.000000000000000000, 0.06496062992125986590, 0.000000000000000000 ) ) ;
#9290=DIRECTION ( 'NONE',  ( 0.000000000000000000, 1.000000000000000000, 0.000000000000000000 ) ) ;
#9299=CARTESIAN_POINT ( 'NONE',  ( -0.1022864650139100884, 0.000000000000000000, -1.048351444896847144E-20 ) ) ;
#9311=ORIENTED_EDGE ( 'NONE', *, *, #14570, .T. ) ;
#9331=EDGE_LOOP ( 'NONE', ( #13770, #7109, #12020, #12470 ) ) ;
#9339=DIRECTION ( 'NONE',  ( 0.000000000000000000, 0.000000000000000000, 1.000000000000000000 ) ) ;
#9407=AXIS2_PLACEMENT_3D ( 'NONE', #11886, #7176, #8274 ) ;
#9414=DIRECTION ( 'NONE',  ( 1.224646799147353454E-16, 0.000000000000000000, -1.000000000000000000 ) ) ;
#9454=VECTOR ( 'NONE', #8224, 39.37007874015748143 ) ;
#9458=( CONVERSION_BASED_UNIT ( 'INCH', #5906 ) LENGTH_UNIT ( ) NAMED_UNIT ( #11877 ) );
#9491=CARTESIAN_POINT ( 'NONE',  ( 4.821444091131311524E-18, 0.4133858267716535306, 0.03937007874015747977 ) ) ;
#9501=EDGE_LOOP ( 'NONE', ( #1834, #13799, #5217, #286 ) ) ;
#9515=DIRECTION ( 'NONE',  ( 0.5000000000000001110, 0.000000000000000000, -0.8660254037844385966 ) ) ;
#9545=CARTESIAN_POINT ( 'NONE',  ( 0.000000000000000000, 0.4094488188976377896, 0.000000000000000000 ) ) ;
#9547=CARTESIAN_POINT ( 'NONE',  ( 0.05114323250695499562, 0.05905511811023622659, -0.08858267716535433989 ) ) ;
#9613=MANIFOLD_SOLID_BREP ( 'Boss-Extrude2', #6607 ) ;
#9653=AXIS2_PLACEMENT_3D ( 'NONE', #3271, #14009, #3513 ) ;
#9723=CARTESIAN_POINT ( 'NONE',  ( 0.000000000000000000, 0.05905511811023622659, 0.000000000000000000 ) ) ;
#9726=CARTESIAN_POINT ( 'NONE',  ( 0.000000000000000000, 0.000000000000000000, 0.08858267716535432601 ) ) ;
#9737=EDGE_LOOP ( 'NONE', ( #7198, #15133, #14488 ) ) ;
#9793=DIRECTION ( 'NONE',  ( -0.000000000000000000, -1.000000000000000000, -0.000000000000000000 ) ) ;
#9827=LINE ( 'NONE', #1230, #11357 ) ;
#9851=DIRECTION ( 'NONE',  ( 0.000000000000000000, 1.000000000000000000, 0.000000000000000000 ) ) ;
#9862=VECTOR ( 'NONE', #5607, 39.37007874015749564 ) ;
#9893=ORIENTED_EDGE ( 'NONE', *, *, #1087, .F. ) ;
#9895=CARTESIAN_POINT ( 'NONE',  ( -0.05114323250695503725, 0.05905511811023622659, -0.08858267716535432601 ) ) ;
#9918=CARTESIAN_POINT ( 'NONE',  ( 0.000000000000000000, 0.4094488188976377896, 0.000000000000000000 ) ) ;
#9977=EDGE_CURVE ( 'NONE', #8823, #11277, #1788, .T. ) ;
#10034=DIRECTION ( 'NONE',  ( -1.000000000000000000, -0.000000000000000000, 0.000000000000000000 ) ) ;
#10077=ORIENTED_EDGE ( 'NONE', *, *, #12977, .T. ) ;
#10078=VERTEX_POINT ( 'NONE', #6781 ) ;
#10084=DIRECTION ( 'NONE',  ( -0.5000000000000001110, 0.000000000000000000, 0.8660254037844385966 ) ) ;
#10087=CONICAL_SURFACE ( 'NONE', #584, 0.08858267716535432601, 1.047197551196600074 ) ;
#10127=ORIENTED_EDGE ( 'NONE', *, *, #6432, .F. ) ;
#10129=EDGE_LOOP ( 'NONE', ( #15312, #11105, #14255, #13597 ) ) ;
#10132=DIRECTION ( 'NONE',  ( 1.669238443041289155E-16, -0.000000000000000000, 1.000000000000000000 ) ) ;
#10138=CARTESIAN_POINT ( 'NONE',  ( 0.1022864650139100745, 0.05905511811023622659, 1.563012696487738457E-17 ) ) ;
#10157=DIRECTION ( 'NONE',  ( 1.000000000000000000, 0.000000000000000000, 0.000000000000000000 ) ) ;
#10159=CARTESIAN_POINT ( 'NONE',  ( 4.821444091131311524E-18, 0.4094488188976377896, 0.03937007874015747977 ) ) ;
#10173=CARTESIAN_POINT ( 'NONE',  ( 0.000000000000000000, 0.4133858267716535306, 0.000000000000000000 ) ) ;
#10189=UNCERTAINTY_MEASURE_WITH_UNIT (LENGTH_MEASURE( 1.000000000000000082E-05 ), #13101, 'distance_accuracy_value', 'NONE');
#10195=CARTESIAN_POINT ( 'NONE',  ( 0.000000000000000000, 0.06496062992125986590, 0.04527559055118110520 ) ) ;
#10284=DIRECTION ( 'NONE',  ( 0.000000000000000000, 0.000000000000000000, 1.000000000000000000 ) ) ;
#10286=DIRECTION ( 'NONE',  ( 0.5000000000000002220, 0.000000000000000000, 0.8660254037844384856 ) ) ;
#10287=ORIENTED_EDGE ( 'NONE', *, *, #8077, .F. ) ;
#10293=CARTESIAN_POINT ( 'NONE',  ( 0.1022864650139100745, 0.05905511811023622659, 1.563012696487738457E-17 ) ) ;
#10348=DIMENSIONAL_EXPONENTS ( 1.000000000000000000, 0.000000000000000000, 0.000000000000000000, 0.000000000000000000, 0.000000000000000000, 0.000000000000000000, 0.000000000000000000 ) ;
#10350=DIRECTION ( 'NONE',  ( 0.000000000000000000, -0.4999999999999979461, 0.8660254037844397068 ) ) ;
#10373=EDGE_CURVE ( 'NONE', #1731, #11277, #8746, .T. ) ;
#10383=VECTOR ( 'NONE', #9515, 39.37007874015748143 ) ;
#10396=AXIS2_PLACEMENT_3D ( 'NONE', #4598, #1247, #8135 ) ;
#10399=AXIS2_PLACEMENT_3D ( 'NONE', #566, #10132, #7615 ) ;
#10491=CARTESIAN_POINT ( 'NONE',  ( 0.05114323250695499562, 0.000000000000000000, -0.08858267716535433989 ) ) ;
#10531=PLANE ( 'NONE',  #3182 ) ;
#10559=EDGE_CURVE ( 'NONE', #2689, #12058, #3843, .T. ) ;
#10562=EDGE_LOOP ( 'NONE', ( #13067, #2352, #12852, #9311 ) ) ;
#10567=DIRECTION ( 'NONE',  ( -0.000000000000000000, -1.000000000000000000, -0.000000000000000000 ) ) ;
#10604=CARTESIAN_POINT ( 'NONE',  ( -0.1022864650139100884, 0.05905511811023622659, -1.048351444896847144E-20 ) ) ;
#10643=CARTESIAN_POINT ( 'NONE',  ( 0.05114323250695503031, 0.05905511811023622659, 0.08858267716535433989 ) ) ;
#10689=DIRECTION ( 'NONE',  ( -0.000000000000000000, 1.000000000000000000, 0.000000000000000000 ) ) ;
#10726=ADVANCED_FACE ( 'NONE', ( #6651 ), #8952, .F. ) ;
#10745=ORIENTED_EDGE ( 'NONE', *, *, #5129, .T. ) ;
#10774=FACE_OUTER_BOUND ( 'NONE', #11718, .T. ) ;
#10827=VECTOR ( 'NONE', #6023, 39.37007874015748143 ) ;
#10855=EDGE_CURVE ( 'NONE', #426, #2689, #13166, .T. ) ;
#10860=CIRCLE ( 'NONE', #3108, 0.03937007874015747977 ) ;
#10897=CIRCLE ( 'NONE', #12151, 0.003937007874015749712 ) ;
#10910=AXIS2_PLACEMENT_3D ( 'NONE', #11177, #9851, #6291 ) ;
#10946=FACE_OUTER_BOUND ( 'NONE', #1529, .T. ) ;
#10985=EDGE_CURVE ( 'NONE', #4739, #12623, #1643, .T. ) ;
#11012=CARTESIAN_POINT ( 'NONE',  ( 0.000000000000000000, 0.4094488188976377896, 0.03543307086614173179 ) ) ;
#11018=FACE_OUTER_BOUND ( 'NONE', #1830, .T. ) ;
#11019=VERTEX_POINT ( 'NONE', #9726 ) ;
#11033=CARTESIAN_POINT ( 'NONE',  ( 0.05114323250695503031, 0.05905511811023622659, 0.08858267716535433989 ) ) ;
#11105=ORIENTED_EDGE ( 'NONE', *, *, #14570, .F. ) ;
#11125=DIRECTION ( 'NONE',  ( 0.000000000000000000, 0.000000000000000000, 1.000000000000000000 ) ) ;
#11138=ORIENTED_EDGE ( 'NONE', *, *, #10559, .T. ) ;
#11142=PLANE ( 'NONE',  #653 ) ;
#11177=CARTESIAN_POINT ( 'NONE',  ( 0.000000000000000000, 0.000000000000000000, 0.000000000000000000 ) ) ;
#11183=VECTOR ( 'NONE', #9793, 39.37007874015748143 ) ;
#11253=DIRECTION ( 'NONE',  ( 0.000000000000000000, 1.000000000000000000, 0.000000000000000000 ) ) ;
#11257=ADVANCED_FACE ( 'NONE', ( #8357 ), #4066, .T. ) ;
#11266=CARTESIAN_POINT ( 'NONE',  ( 0.000000000000000000, 0.1692468441617604180, -0.03937007874015747977 ) ) ;
#11277=VERTEX_POINT ( 'NONE', #5924 ) ;
#11281=CARTESIAN_POINT ( 'NONE',  ( 0.000000000000000000, 0.000000000000000000, 0.000000000000000000 ) ) ;
#11317=CARTESIAN_POINT ( 'NONE',  ( 0.000000000000000000, 0.4094488188976377896, 0.000000000000000000 ) ) ;
#11334=DIRECTION ( 'NONE',  ( -0.000000000000000000, 1.000000000000000000, 0.000000000000000000 ) ) ;
#11357=VECTOR ( 'NONE', #4805, 39.37007874015748143 ) ;
#11380=DIRECTION ( 'NONE',  ( -0.000000000000000000, -1.000000000000000000, -0.000000000000000000 ) ) ;
#11473=CARTESIAN_POINT ( 'NONE',  ( -0.05114323250695500950, 0.000000000000000000, 0.08858267716535433989 ) ) ;
#11474=CARTESIAN_POINT ( 'NONE',  ( 0.05114323250695503031, 0.05905511811023622659, 0.08858267716535433989 ) ) ;
#11476=LINE ( 'NONE', #10138, #13925 ) ;
#11481=AXIS2_PLACEMENT_3D ( 'NONE', #12576, #4264, #5441 ) ;
#11485=ORIENTED_EDGE ( 'NONE', *, *, #8077, .T. ) ;
#11489=CARTESIAN_POINT ( 'NONE',  ( -0.05114323250695500950, 0.000000000000000000, 0.08858267716535433989 ) ) ;
#11491=LINE ( 'NONE', #821, #4652 ) ;
#11539=CARTESIAN_POINT ( 'NONE',  ( -0.1022864650139100884, 0.05905511811023622659, -1.048351444896847144E-20 ) ) ;
#11540=VERTEX_POINT ( 'NONE', #10159 ) ;
#11543=ADVANCED_FACE ( 'NONE', ( #5274 ), #10087, .T. ) ;
#11552=DIRECTION ( 'NONE',  ( 0.000000000000000000, 0.000000000000000000, 1.000000000000000000 ) ) ;
#11558=CARTESIAN_POINT ( 'NONE',  ( 0.000000000000000000, 0.4133858267716535306, 0.000000000000000000 ) ) ;
#11617=CIRCLE ( 'NONE', #8618, 0.04527559055118110520 ) ;
#11671=LINE ( 'NONE', #10491, #1400 ) ;
#11672=DIMENSIONAL_EXPONENTS ( 1.000000000000000000, 0.000000000000000000, 0.000000000000000000, 0.000000000000000000, 0.000000000000000000, 0.000000000000000000, 0.000000000000000000 ) ;
#11718=EDGE_LOOP ( 'NONE', ( #9015, #8317, #11891 ) ) ;
#11842=EDGE_LOOP ( 'NONE', ( #13675, #2129, #15435, #9893 ) ) ;
#11863=LENGTH_MEASURE_WITH_UNIT ( LENGTH_MEASURE( 0.02539999999999999897 ), #12960 );
#11877=DIMENSIONAL_EXPONENTS ( 1.000000000000000000, 0.000000000000000000, 0.000000000000000000, 0.000000000000000000, 0.000000000000000000, 0.000000000000000000, 0.000000000000000000 ) ;
#11886=CARTESIAN_POINT ( 'NONE',  ( 0.000000000000000000, 0.000000000000000000, 0.000000000000000000 ) ) ;
#11891=ORIENTED_EDGE ( 'NONE', *, *, #12409, .T. ) ;
#11925=CIRCLE ( 'NONE', #6377, 0.003937007874015749712 ) ;
#11941=CARTESIAN_POINT ( 'NONE',  ( 0.000000000000000000, 0.06496062992125986590, 0.000000000000000000 ) ) ;
#11973=CARTESIAN_POINT ( 'NONE',  ( -1.084824920504545016E-17, 0.000000000000000000, -0.08858267716535432601 ) ) ;
#12013=LINE ( 'NONE', #1273, #10827 ) ;
#12020=ORIENTED_EDGE ( 'NONE', *, *, #10985, .T. ) ;
#12053=LINE ( 'NONE', #9547, #9454 ) ;
#12058=VERTEX_POINT ( 'NONE', #1751 ) ;
#12090=EDGE_CURVE ( 'NONE', #1174, #1730, #11617, .T. ) ;
#12151=AXIS2_PLACEMENT_3D ( 'NONE', #7981, #15194, #7598 ) ;
#12167=DIRECTION ( 'NONE',  ( -0.000000000000000000, -1.000000000000000000, -0.000000000000000000 ) ) ;
#12173=VECTOR ( 'NONE', #10350, 39.37007874015748854 ) ;
#12183=FACE_OUTER_BOUND ( 'NONE', #7903, .T. ) ;
#12230=EDGE_CURVE ( 'NONE', #4739, #4286, #1077, .T. ) ;
#12254=EDGE_CURVE ( 'NONE', #10078, #12623, #10860, .T. ) ;
#12308=CARTESIAN_POINT ( 'NONE',  ( 0.000000000000000000, 0.000000000000000000, 0.000000000000000000 ) ) ;
#12409=EDGE_CURVE ( 'NONE', #2631, #11019, #5608, .T. ) ;
#12470=ORIENTED_EDGE ( 'NONE', *, *, #4928, .T. ) ;
#12493=PRODUCT_CONTEXT ( 'NONE', #3292, 'mechanical' ) ;
#12533=LINE ( 'NONE', #4761, #6877 ) ;
#12576=CARTESIAN_POINT ( 'NONE',  ( 0.000000000000000000, 0.000000000000000000, 0.000000000000000000 ) ) ;
#12585=AXIS2_PLACEMENT_3D ( 'NONE', #9545, #7101, #3442 ) ;
#12623=VERTEX_POINT ( 'NONE', #4774 ) ;
#12668=DIRECTION ( 'NONE',  ( -0.000000000000000000, -1.000000000000000000, -0.000000000000000000 ) ) ;
#12725=CARTESIAN_POINT ( 'NONE',  ( 0.000000000000000000, 0.4133858267716535306, 0.000000000000000000 ) ) ;
#12788=DIRECTION ( 'NONE',  ( -0.000000000000000000, -1.000000000000000000, -0.000000000000000000 ) ) ;
#12791=DIRECTION ( 'NONE',  ( -0.000000000000000000, 1.000000000000000000, 0.000000000000000000 ) ) ;
#12808=CARTESIAN_POINT ( 'NONE',  ( 0.000000000000000000, 0.4094488188976377896, -0.03937007874015747977 ) ) ;
#12812=DIRECTION ( 'NONE',  ( 0.000000000000000000, 0.000000000000000000, -1.000000000000000000 ) ) ;
#12844=FACE_OUTER_BOUND ( 'NONE', #1480, .T. ) ;
#12852=ORIENTED_EDGE ( 'NONE', *, *, #10855, .F. ) ;
#12861=CARTESIAN_POINT ( 'NONE',  ( 0.000000000000000000, 0.000000000000000000, 0.08858267716535432601 ) ) ;
#12926=EDGE_LOOP ( 'NONE', ( #6235, #5232, #7715, #7559, #5435, #814 ) ) ;
#12960=( LENGTH_UNIT ( ) NAMED_UNIT ( * ) SI_UNIT ( $, .METRE. ) );
#12969=TOROIDAL_SURFACE ( 'NONE', #5687, 0.04527559055118110520, 0.005905511811023621965 ) ;
#12977=EDGE_CURVE ( 'NONE', #14826, #748, #4882, .T. ) ;
#12980=PLANE ( 'NONE',  #2858 ) ;
#13067=ORIENTED_EDGE ( 'NONE', *, *, #8727, .T. ) ;
#13101=( CONVERSION_BASED_UNIT ( 'INCH', #11863 ) LENGTH_UNIT ( ) NAMED_UNIT ( #11672 ) );
#13166=LINE ( 'NONE', #4706, #3959 ) ;
#13199=EDGE_CURVE ( 'NONE', #11540, #14826, #11925, .T. ) ;
#13284=( BOUNDED_CURVE ( )  B_SPLINE_CURVE ( 3, ( #2550, #8814, #6381, #2722 ),
 .UNSPECIFIED., .F., .T. ) 
 B_SPLINE_CURVE_WITH_KNOTS ( ( 4, 4 ),
 ( 1.570796326794896780, 4.712388980384689674 ),
 .UNSPECIFIED. ) 
 CURVE ( )  GEOMETRIC_REPRESENTATION_ITEM ( )  RATIONAL_B_SPLINE_CURVE ( ( 1.000000000000000000, 0.3333333333333333703, 0.3333333333333333703, 1.000000000000000000 ) ) 
 REPRESENTATION_ITEM ( '' )  );
#13294=ORIENTED_EDGE ( 'NONE', *, *, #1214, .F. ) ;
#13299=DIRECTION ( 'NONE',  ( 0.000000000000000000, -1.000000000000000000, -0.000000000000000000 ) ) ;
#13425=DIRECTION ( 'NONE',  ( 1.000000000000000000, 0.000000000000000000, 0.000000000000000000 ) ) ;
#13449=DIRECTION ( 'NONE',  ( 0.000000000000000000, 0.000000000000000000, 1.000000000000000000 ) ) ;
#13453=( GEOMETRIC_REPRESENTATION_CONTEXT ( 3 ) GLOBAL_UNCERTAINTY_ASSIGNED_CONTEXT ( ( #10189 ) ) GLOBAL_UNIT_ASSIGNED_CONTEXT ( ( #13101, #15153, #4493 ) ) REPRESENTATION_CONTEXT ( 'NONE', 'WORKASPACE' ) );
#13510=EDGE_CURVE ( 'NONE', #3814, #113, #11476, .T. ) ;
#13523=ORIENTED_EDGE ( 'NONE', *, *, #1214, .T. ) ;
#13551=VERTEX_POINT ( 'NONE', #8975 ) ;
#13585=DIRECTION ( 'NONE',  ( 0.000000000000000000, 0.000000000000000000, 1.000000000000000000 ) ) ;
#13597=ORIENTED_EDGE ( 'NONE', *, *, #13510, .T. ) ;
#13635=AXIS2_PLACEMENT_3D ( 'NONE', #9251, #7917, #4470 ) ;
#13639=CARTESIAN_POINT ( 'NONE',  ( 0.1022864650139100745, 0.000000000000000000, 1.563012696487738457E-17 ) ) ;
#13675=ORIENTED_EDGE ( 'NONE', *, *, #5853, .F. ) ;
#13693=VECTOR ( 'NONE', #2741, 39.37007874015748143 ) ;
#13745=SHAPE_DEFINITION_REPRESENTATION ( #775, #7785 ) ;
#13749=CARTESIAN_POINT ( 'NONE',  ( 0.000000000000000000, 0.05114323250695475970, 0.000000000000000000 ) ) ;
#13753=ORIENTED_EDGE ( 'NONE', *, *, #12090, .F. ) ;
#13762=CARTESIAN_POINT ( 'NONE',  ( 0.000000000000000000, 0.000000000000000000, 0.000000000000000000 ) ) ;
#13763=DIRECTION ( 'NONE',  ( -0.5000000000000001110, 0.000000000000000000, -0.8660254037844384856 ) ) ;
#13770=ORIENTED_EDGE ( 'NONE', *, *, #4642, .F. ) ;
#13799=ORIENTED_EDGE ( 'NONE', *, *, #4642, .T. ) ;
#13858=CIRCLE ( 'NONE', #8100, 0.03543307086614173179 ) ;
#13912=( NAMED_UNIT ( * ) SI_UNIT ( $, .STERADIAN. ) SOLID_ANGLE_UNIT ( ) );
#13925=VECTOR ( 'NONE', #4254, 39.37007874015748143 ) ;
#13938=ORIENTED_EDGE ( 'NONE', *, *, #8641, .F. ) ;
#13946=EDGE_LOOP ( 'NONE', ( #10077, #7480 ) ) ;
#13967=VECTOR ( 'NONE', #12167, 39.37007874015748143 ) ;
#14004=APPLICATION_CONTEXT ( 'automotive_design' ) ;
#14009=DIRECTION ( 'NONE',  ( 0.000000000000000000, 1.000000000000000000, 0.000000000000000000 ) ) ;
#14066=DIRECTION ( 'NONE',  ( 0.000000000000000000, -0.000000000000000000, 1.000000000000000000 ) ) ;
#14130=FACE_BOUND ( 'NONE', #6470, .T. ) ;
#14134=VECTOR ( 'NONE', #10286, 39.37007874015749564 ) ;
#14147=( LENGTH_UNIT ( ) NAMED_UNIT ( * ) SI_UNIT ( $, .METRE. ) );
#14153=DIRECTION ( 'NONE',  ( 0.000000000000000000, 0.000000000000000000, -1.000000000000000000 ) ) ;
#14246=EDGE_CURVE ( 'NONE', #8823, #3814, #14742, .T. ) ;
#14255=ORIENTED_EDGE ( 'NONE', *, *, #6268, .F. ) ;
#14259=LINE ( 'NONE', #9491, #7862 ) ;
#14277=CARTESIAN_POINT ( 'NONE',  ( 4.821444091131311524E-18, 0.1692468441617604180, 0.03937007874015747977 ) ) ;
#14368=CARTESIAN_POINT ( 'NONE',  ( 4.580371886574746102E-18, 0.4133858267716535306, -0.03543307086614173179 ) ) ;
#14381=AXIS2_PLACEMENT_3D ( 'NONE', #1001, #5747, #14153 ) ;
#14398=CARTESIAN_POINT ( 'NONE',  ( 0.000000000000000000, 0.06496062992125986590, 0.000000000000000000 ) ) ;
#14446=ORIENTED_EDGE ( 'NONE', *, *, #5954, .F. ) ;
#14478=( GEOMETRIC_REPRESENTATION_CONTEXT ( 3 ) GLOBAL_UNCERTAINTY_ASSIGNED_CONTEXT ( ( #14896 ) ) GLOBAL_UNIT_ASSIGNED_CONTEXT ( ( #9458, #2069, #13912 ) ) REPRESENTATION_CONTEXT ( 'NONE', 'WORKASPACE' ) );
#14488=ORIENTED_EDGE ( 'NONE', *, *, #6002, .T. ) ;
#14570=EDGE_CURVE ( 'NONE', #426, #7319, #12053, .T. ) ;
#14587=( NAMED_UNIT ( * ) SI_UNIT ( $, .STERADIAN. ) SOLID_ANGLE_UNIT ( ) );
#14728=MANIFOLD_SOLID_BREP ( 'Split Line1', #2859 ) ;
#14742=LINE ( 'NONE', #11033, #13693 ) ;
#14826=VERTEX_POINT ( 'NONE', #2522 ) ;
#14869=AXIS2_PLACEMENT_3D ( 'NONE', #9918, #672, #4100 ) ;
#14896=UNCERTAINTY_MEASURE_WITH_UNIT (LENGTH_MEASURE( 1.000000000000000082E-05 ), #9458, 'distance_accuracy_value', 'NONE');
#14901=LINE ( 'NONE', #13639, #3345 ) ;
#14927=CONICAL_SURFACE ( 'NONE', #9407, 0.08858267716535432601, 1.047197551196600074 ) ;
#15073=DIRECTION ( 'NONE',  ( 0.8660254037844385966, 0.000000000000000000, -0.5000000000000003331 ) ) ;
#15090=EDGE_LOOP ( 'NONE', ( #13938, #13294, #6614, #1998 ) ) ;
#15098=FACE_OUTER_BOUND ( 'NONE', #3124, .T. ) ;
#15117=CIRCLE ( 'NONE', #3113, 0.03937007874015747977 ) ;
#15133=ORIENTED_EDGE ( 'NONE', *, *, #6530, .T. ) ;
#15153=( NAMED_UNIT ( * ) PLANE_ANGLE_UNIT ( ) SI_UNIT ( $, .RADIAN. ) );
#15194=DIRECTION ( 'NONE',  ( 1.000000000000000000, -0.000000000000000000, 1.224646799147353207E-16 ) ) ;
#15312=ORIENTED_EDGE ( 'NONE', *, *, #4359, .T. ) ;
#15332=ADVANCED_FACE ( 'NONE', ( #8578 ), #12969, .F. ) ;
#15379=CARTESIAN_POINT ( 'NONE',  ( -0.07874015748031494566, 0.1685051786281938357, -0.03937007874015750752 ) ) ;
#15386=DIRECTION ( 'NONE',  ( 0.000000000000000000, -0.000000000000000000, 1.000000000000000000 ) ) ;
#15391=AXIS2_PLACEMENT_3D ( 'NONE', #10173, #7563, #9002 ) ;
#15394=DIRECTION ( 'NONE',  ( -0.5000000000000002220, 0.000000000000000000, -0.8660254037844384856 ) ) ;
#15435=ORIENTED_EDGE ( 'NONE', *, *, #1981, .T. ) ;
#15527=COLOUR_RGB('Black',0.12,0.14,0.17);
#15528=FILL_AREA_STYLE_COLOUR('',#15527);
#15529=FILL_AREA_STYLE('',(#15528));
#15530=SURFACE_STYLE_FILL_AREA(#15529);
#15531=SURFACE_SIDE_STYLE('',(#15530));
#15532=SURFACE_STYLE_USAGE(.BOTH.,#15531);
#15533=PRESENTATION_STYLE_ASSIGNMENT((#15532));
ENDSEC;
END-ISO-10303-21;
